ISO-10303-21;
HEADER;
FILE_DESCRIPTION (('STEP AP214'),
    '1' );
FILE_NAME ('Part10^Assembly Drive shaft gear.step',
    '2026-10-22T18:53:08',
    ( '' ),
    ( '' ),
    'SwSTEP 2.0',
    'SolidWorks 2025',
    '' );
FILE_SCHEMA (( 'AUTOMOTIVE_DESIGN' ));
ENDSEC;

DATA;
#21=EDGE_CURVE ( 'NONE', #19190, #16784, #8531, .T. ) ;
#43=PRODUCT ( 'Part10^Assembly Drive shaft gear', 'Part10^Assembly Drive shaft gear', '', ( #22523 ) ) ;
#78=ORIENTED_EDGE ( 'NONE', *, *, #6210, .T. ) ;
#96=EDGE_CURVE ( 'NONE', #2943, #5490, #6588, .T. ) ;
#111=ORIENTED_EDGE ( 'NONE', *, *, #20184, .F. ) ;
#192=VERTEX_POINT ( 'NONE', #13627 ) ;
#194=DIRECTION ( 'NONE',  ( 0.000000000000000000, 0.000000000000000000, -1.000000000000000000 ) ) ;
#281=CARTESIAN_POINT ( 'NONE',  ( 9.324366632326096311E-16, 9.000000000000000000, 77.99999999999998579 ) ) ;
#298=ORIENTED_EDGE ( 'NONE', *, *, #19273, .F. ) ;
#325=CARTESIAN_POINT ( 'NONE',  ( -2.999999999999999112, 111.0000000000000000, 80.99999999999998579 ) ) ;
#388=CARTESIAN_POINT ( 'NONE',  ( -2.979928582684572724, 8.492451671845357097, 80.60107722653498286 ) ) ;
#405=DIRECTION ( 'NONE',  ( 0.000000000000000000, 1.000000000000000000, 0.000000000000000000 ) ) ;
#537=ADVANCED_FACE ( 'NONE', ( #2678 ), #12172, .T. ) ;
#614=DIRECTION ( 'NONE',  ( 0.000000000000000000, -0.000000000000000000, 1.000000000000000000 ) ) ;
#619=DIRECTION ( 'NONE',  ( 0.000000000000000000, 0.000000000000000000, 1.000000000000000000 ) ) ;
#640=CARTESIAN_POINT ( 'NONE',  ( -0.7829208760733560313, 8.967963617333239768, 78.09729311758064796 ) ) ;
#739=FACE_OUTER_BOUND ( 'NONE', #4967, .T. ) ;
#769=CIRCLE ( 'NONE', #3875, 9.000000000000000000 ) ;
#840=ADVANCED_FACE ( 'NONE', ( #11965, #19433 ), #4926, .T. ) ;
#950=EDGE_LOOP ( 'NONE', ( #1693, #8351, #298, #18257 ) ) ;
#1007=STYLED_ITEM('',(#24155),#2970);
#1145=CLOSED_SHELL ( 'NONE', ( #17694, #13029, #8993, #840, #11472, #14015, #20301, #5214, #16715, #7143, #23558, #13583, #21732, #537 ) ) ;
#1154=CARTESIAN_POINT ( 'NONE',  ( -2.999999999999995559, 8.485281374238571317, 105.0000000000000000 ) ) ;
#1199=CARTESIAN_POINT ( 'NONE',  ( 0.3943934708257424981, 8.993434178613792795, 101.9804670325896012 ) ) ;
#1469=VERTEX_POINT ( 'NONE', #5637 ) ;
#1576=SHAPE_REPRESENTATION_RELATIONSHIP ( 'NONE' , 'NONE' ,  #17018, #13375 ) ;
#1614=EDGE_CURVE ( 'NONE', #16055, #16900, #21108, .T. ) ;
#1693=ORIENTED_EDGE ( 'NONE', *, *, #6210, .F. ) ;
#1918=LINE ( 'NONE', #3755, #22402 ) ;
#2062=LINE ( 'NONE', #16946, #2122 ) ;
#2122=VECTOR ( 'NONE', #22114, 1000.000000000000000 ) ;
#2130=VECTOR ( 'NONE', #11900, 1000.000000000000000 ) ;
#2174=CARTESIAN_POINT ( 'NONE',  ( 3.000000000000002665, 6.000000000000000000, 98.99999999999998579 ) ) ;
#2212=CIRCLE ( 'NONE', #14681, 9.000000000000000000 ) ;
#2213=CARTESIAN_POINT ( 'NONE',  ( 2.601280481040925796, 8.616622289297277248, 79.49281377527864834 ) ) ;
#2237=ORIENTED_EDGE ( 'NONE', *, *, #4058, .F. ) ;
#2306=FACE_OUTER_BOUND ( 'NONE', #16209, .T. ) ;
#2359=ORIENTED_EDGE ( 'NONE', *, *, #22600, .T. ) ;
#2436=PLANE ( 'NONE',  #19714 ) ;
#2450=CARTESIAN_POINT ( 'NONE',  ( -1.984007748668716653, 8.779741040573222577, 78.74128913175751165 ) ) ;
#2509=ORIENTED_EDGE ( 'NONE', *, *, #8040, .F. ) ;
#2514=EDGE_LOOP ( 'NONE', ( #8664, #78 ) ) ;
#2588=CARTESIAN_POINT ( 'NONE',  ( -0.3972991690984661317, 8.993302502987313929, 78.01992857238796830 ) ) ;
#2647=CARTESIAN_POINT ( 'NONE',  ( 9.000000000000000000, 1.102182119232617714E-15, 105.0000000000000000 ) ) ;
#2678=FACE_OUTER_BOUND ( 'NONE', #3876, .T. ) ;
#2690=EDGE_CURVE ( 'NONE', #16784, #16942, #13922, .T. ) ;
#2750=DIRECTION ( 'NONE',  ( 0.000000000000000000, -1.000000000000000000, 0.000000000000000000 ) ) ;
#2905=CARTESIAN_POINT ( 'NONE',  ( -0.3960160581560826509, 8.993383190415354278, 101.9803173862455310 ) ) ;
#2943=VERTEX_POINT ( 'NONE', #14626 ) ;
#2970=MANIFOLD_SOLID_BREP ( 'Cut-Extrude1', #1145 ) ;
#3006=LINE ( 'NONE', #17765, #11238 ) ;
#3065=CARTESIAN_POINT ( 'NONE',  ( -7.999999999999992895, 0.000000000000000000, 105.0000000000000000 ) ) ;
#3077=CARTESIAN_POINT ( 'NONE',  ( -9.000000000000000000, 0.000000000000000000, 105.0000000000000000 ) ) ;
#3105=ORIENTED_EDGE ( 'NONE', *, *, #12078, .T. ) ;
#3123=DIRECTION ( 'NONE',  ( 0.000000000000000000, 0.000000000000000000, 1.000000000000000000 ) ) ;
#3195=FACE_OUTER_BOUND ( 'NONE', #13125, .T. ) ;
#3206=PRODUCT_DEFINITION_SHAPE ( 'NONE', 'NONE',  #21247 ) ;
#3210=ORIENTED_EDGE ( 'NONE', *, *, #1614, .F. ) ;
#3255=CARTESIAN_POINT ( 'NONE',  ( 0.1940582010532044821, 9.000069240190681441, 102.0002077206765563 ) ) ;
#3361=DIRECTION ( 'NONE',  ( 1.000000000000000000, 0.000000000000000000, 0.000000000000000000 ) ) ;
#3430=EDGE_LOOP ( 'NONE', ( #22104, #16123, #16319, #22986 ) ) ;
#3477=CARTESIAN_POINT ( 'NONE',  ( 0.000000000000000000, 0.000000000000000000, 105.0000000000000000 ) ) ;
#3591=CARTESIAN_POINT ( 'NONE',  ( 9.324366623732823450E-16, 111.0000000000000000, 80.99999999999998579 ) ) ;
#3696=AXIS2_PLACEMENT_3D ( 'NONE', #18669, #7201, #16459 ) ;
#3735=EDGE_CURVE ( 'NONE', #1469, #21201, #769, .T. ) ;
#3755=CARTESIAN_POINT ( 'NONE',  ( -2.999999999999999112, 111.0000000000000000, 80.99999999999998579 ) ) ;
#3792=EDGE_CURVE ( 'NONE', #6922, #16055, #3006, .T. ) ;
#3875=AXIS2_PLACEMENT_3D ( 'NONE', #19230, #6422, #17885 ) ;
#3876=EDGE_LOOP ( 'NONE', ( #18717, #19465, #21892, #19014, #11409 ) ) ;
#3980=AXIS2_PLACEMENT_3D ( 'NONE', #16419, #7161, #19869 ) ;
#3983=CARTESIAN_POINT ( 'NONE',  ( 9.000000000000000000, 1.102182119232617714E-15, 103.9999999999999858 ) ) ;
#4019=ORIENTED_EDGE ( 'NONE', *, *, #18486, .F. ) ;
#4030=FACE_OUTER_BOUND ( 'NONE', #2514, .T. ) ;
#4043=CARTESIAN_POINT ( 'NONE',  ( 2.903090122117997218, 8.519021868010421272, 80.21852650458262701 ) ) ;
#4049=CARTESIAN_POINT ( 'NONE',  ( -2.382914664853783560, 8.679543164111374054, 79.16706182717918239 ) ) ;
#4058=EDGE_CURVE ( 'NONE', #6887, #9582, #2212, .T. ) ;
#4089=ORIENTED_EDGE ( 'NONE', *, *, #12668, .F. ) ;
#4115=LINE ( 'NONE', #20951, #13285 ) ;
#4152=PLANE ( 'NONE',  #12609 ) ;
#4178=CARTESIAN_POINT ( 'NONE',  ( 0.9720249034408605660, 8.949203418382943198, 78.15512200942710308 ) ) ;
#4182=CARTESIAN_POINT ( 'NONE',  ( 9.324366623732823450E-16, 6.000000000000000000, 80.99999999999998579 ) ) ;
#4338=EDGE_CURVE ( 'NONE', #21201, #1469, #12599, .T. ) ;
#4373=CARTESIAN_POINT ( 'NONE',  ( 3.000000000000000888, 6.000000000000000000, 80.99999999999998579 ) ) ;
#4383=CIRCLE ( 'NONE', #9407, 7.999999999999992895 ) ;
#4401=DIRECTION ( 'NONE',  ( -1.000000000000000000, 0.000000000000000000, 9.637352644315592778E-17 ) ) ;
#4519=DIRECTION ( 'NONE',  ( 0.000000000000000000, -1.000000000000000000, 0.000000000000000000 ) ) ;
#4532=AXIS2_PLACEMENT_3D ( 'NONE', #3477, #12620, #20085 ) ;
#4539=FACE_OUTER_BOUND ( 'NONE', #12573, .T. ) ;
#4625=CARTESIAN_POINT ( 'NONE',  ( 1.333298728199530769, 8.902595189562054756, 101.6946980188053118 ) ) ;
#4645=CARTESIAN_POINT ( 'NONE',  ( 9.324366623732823450E-16, 6.000000000000000000, 80.99999999999998579 ) ) ;
#4766=CARTESIAN_POINT ( 'NONE',  ( 7.999999999999992895, 1.040949779275249943E-15, 105.0000000000000000 ) ) ;
#4821=DIRECTION ( 'NONE',  ( 0.000000000000000000, 0.000000000000000000, 1.000000000000000000 ) ) ;
#4859=DIRECTION ( 'NONE',  ( -0.7071067811865493491, 8.659560562354955045E-17, 0.7071067811865456854 ) ) ;
#4871=CARTESIAN_POINT ( 'NONE',  ( 2.901639506146888703, 8.519518907301963040, 99.78718033059439563 ) ) ;
#4891=ORIENTED_EDGE ( 'NONE', *, *, #2690, .F. ) ;
#4926=CYLINDRICAL_SURFACE ( 'NONE', #19191, 9.000000000000000000 ) ;
#4951=VECTOR ( 'NONE', #20876, 1000.000000000000000 ) ;
#4967=EDGE_LOOP ( 'NONE', ( #22817, #9798, #3210, #5662 ) ) ;
#4974=DIRECTION ( 'NONE',  ( -0.000000000000000000, -0.000000000000000000, -1.000000000000000000 ) ) ;
#5157=CARTESIAN_POINT ( 'NONE',  ( 0.000000000000000000, 0.000000000000000000, 105.0000000000000000 ) ) ;
#5192=CIRCLE ( 'NONE', #14536, 3.000000000000002665 ) ;
#5214=ADVANCED_FACE ( 'NONE', ( #9015 ), #14209, .T. ) ;
#5248=EDGE_CURVE ( 'NONE', #23000, #16942, #2062, .T. ) ;
#5318=CARTESIAN_POINT ( 'NONE',  ( 0.000000000000000000, 0.000000000000000000, 0.000000000000000000 ) ) ;
#5322=DIRECTION ( 'NONE',  ( 0.000000000000000000, 1.000000000000000000, 0.000000000000000000 ) ) ;
#5377=LINE ( 'NONE', #20498, #6646 ) ;
#5433=FACE_OUTER_BOUND ( 'NONE', #3430, .T. ) ;
#5438=ORIENTED_EDGE ( 'NONE', *, *, #20665, .T. ) ;
#5490=VERTEX_POINT ( 'NONE', #22990 ) ;
#5503=CARTESIAN_POINT ( 'NONE',  ( -2.999999999999999112, 6.000000000000000000, 80.99999999999998579 ) ) ;
#5551=SHAPE_DEFINITION_REPRESENTATION ( #3206, #17018 ) ;
#5637=CARTESIAN_POINT ( 'NONE',  ( -9.000000000000000000, 0.000000000000000000, 0.9999999999999731326 ) ) ;
#5659=B_SPLINE_CURVE_WITH_KNOTS ( 'NONE', 3,
 ( #14235, #23297, #15836, #8508, #14347, #6927, #8383, #6686, #8861, #14117, #21807, #23411, #12148, #2905, #21336, #3255, #1199, #6809, #19863, #4625, #10454, #19500, #15948, #21577, #10684, #19627, #18155, #12025, #4871, #12404, #17653, #6450 ),
 .UNSPECIFIED., .F., .F.,
 ( 4, 2, 2, 2, 2, 2, 2, 2, 2, 2, 2, 2, 2, 2, 2, 4 ),
 ( 0.000000000000000000, 0.0005902259033179341197, 0.001180451806635868239, 0.001770677709953802359, 0.002360903613271736479, 0.003541355419907607320, 0.004131581323225543174, 0.004721807226543479029, 0.005312033129861415751, 0.005902259033179352472, 0.006492484936497288327, 0.007082710839815223314, 0.007672936743133159168, 0.008263162646451095023, 0.008853388549769029142, 0.009443614453086964997 ),
 .UNSPECIFIED. ) ;
#5662=ORIENTED_EDGE ( 'NONE', *, *, #3792, .F. ) ;
#5664=AXIS2_PLACEMENT_3D ( 'NONE', #12551, #16344, #16112 ) ;
#5696=CARTESIAN_POINT ( 'NONE',  ( 0.000000000000000000, 0.000000000000000000, 0.9999999999999731326 ) ) ;
#5709=ORIENTED_EDGE ( 'NONE', *, *, #8040, .T. ) ;
#5758=CARTESIAN_POINT ( 'NONE',  ( 3.000000000000000888, 6.000000000000000000, 80.99999999999998579 ) ) ;
#5763=CARTESIAN_POINT ( 'NONE',  ( -3.000000000000000444, 8.485281374238569541, 80.80041615069272609 ) ) ;
#5844=DIRECTION ( 'NONE',  ( 1.000000000000000000, 0.000000000000000000, -0.000000000000000000 ) ) ;
#5925=CARTESIAN_POINT ( 'NONE',  ( -9.000000000000000000, 0.000000000000000000, 103.9999999999999858 ) ) ;
#5978=CARTESIAN_POINT ( 'NONE',  ( 0.000000000000000000, 0.000000000000000000, 0.000000000000000000 ) ) ;
#5992=CARTESIAN_POINT ( 'NONE',  ( 9.324366632326096311E-16, 9.000000000000000000, 77.99999999999998579 ) ) ;
#6051=DIRECTION ( 'NONE',  ( -0.000000000000000000, -0.000000000000000000, 1.000000000000000000 ) ) ;
#6092=PRODUCT_DEFINITION_FORMATION_WITH_SPECIFIED_SOURCE ( 'ANY', '', #43, .NOT_KNOWN. ) ;
#6210=EDGE_CURVE ( 'NONE', #14101, #10129, #4383, .T. ) ;
#6221=CARTESIAN_POINT ( 'NONE',  ( -2.999999999999999112, 6.000000000000000000, 80.99999999999998579 ) ) ;
#6262=FACE_OUTER_BOUND ( 'NONE', #7918, .T. ) ;
#6349=DIRECTION ( 'NONE',  ( -0.000000000000000000, -0.000000000000000000, 1.000000000000000000 ) ) ;
#6378=DIRECTION ( 'NONE',  ( -0.000000000000000000, -0.000000000000000000, -1.000000000000000000 ) ) ;
#6383=ORIENTED_EDGE ( 'NONE', *, *, #10862, .F. ) ;
#6422=DIRECTION ( 'NONE',  ( -0.000000000000000000, -0.000000000000000000, 1.000000000000000000 ) ) ;
#6450=CARTESIAN_POINT ( 'NONE',  ( 3.000000000000003109, 8.485281374238567764, 98.99999999999998579 ) ) ;
#6475=EDGE_LOOP ( 'NONE', ( #2509, #6383, #21369, #4089, #15299 ) ) ;
#6588=B_SPLINE_CURVE_WITH_KNOTS ( 'NONE', 3,
 ( #281, #22589, #2588, #640, #13296, #9639, #11698, #13179, #2450, #16834, #4049, #15235, #22487, #17085, #20638, #388, #5763, #20893 ),
 .UNSPECIFIED., .F., .F.,
 ( 4, 2, 2, 2, 2, 2, 2, 2, 4 ),
 ( 0.004724984058646233484, 0.005314812857951324923, 0.005904641657256416362, 0.006494470456561507801, 0.007084299255866599240, 0.007674128055171690679, 0.008263956854476782118, 0.008853785653781873557, 0.009443614453086964997 ),
 .UNSPECIFIED. ) ;
#6646=VECTOR ( 'NONE', #16342, 1000.000000000000000 ) ;
#6686=CARTESIAN_POINT ( 'NONE',  ( -2.384317694982191593, 8.679161036964110565, 100.8311869460038253 ) ) ;
#6809=CARTESIAN_POINT ( 'NONE',  ( 0.7803738342988795207, 8.968189405539467529, 101.9034025936691990 ) ) ;
#6860=DIRECTION ( 'NONE',  ( -0.000000000000000000, -0.000000000000000000, -1.000000000000000000 ) ) ;
#6887=VERTEX_POINT ( 'NONE', #3983 ) ;
#6922=VERTEX_POINT ( 'NONE', #9698 ) ;
#6927=CARTESIAN_POINT ( 'NONE',  ( -2.693951614862269306, 8.587718935426160272, 100.3346014426491877 ) ) ;
#6984=EDGE_CURVE ( 'NONE', #16942, #16055, #5192, .T. ) ;
#7143=ADVANCED_FACE ( 'NONE', ( #5433 ), #7600, .F. ) ;
#7161=DIRECTION ( 'NONE',  ( 0.000000000000000000, 0.000000000000000000, -1.000000000000000000 ) ) ;
#7201=DIRECTION ( 'NONE',  ( -0.000000000000000000, -0.000000000000000000, 1.000000000000000000 ) ) ;
#7212=AXIS2_PLACEMENT_3D ( 'NONE', #21018, #405, #7811 ) ;
#7239=EDGE_LOOP ( 'NONE', ( #14860, #19511, #23094, #23331 ) ) ;
#7270=AXIS2_PLACEMENT_3D ( 'NONE', #21271, #6378, #19439 ) ;
#7324=CARTESIAN_POINT ( 'NONE',  ( 3.000000000000000888, 8.485281374238567764, 80.99999999999998579 ) ) ;
#7359=DIRECTION ( 'NONE',  ( 0.000000000000000000, 0.000000000000000000, -1.000000000000000000 ) ) ;
#7499=VECTOR ( 'NONE', #22026, 1000.000000000000000 ) ;
#7573=ORIENTED_EDGE ( 'NONE', *, *, #3792, .T. ) ;
#7600=CYLINDRICAL_SURFACE ( 'NONE', #10643, 3.000000000000002665 ) ;
#7613=( GEOMETRIC_REPRESENTATION_CONTEXT ( 3 ) GLOBAL_UNCERTAINTY_ASSIGNED_CONTEXT ( ( #8612 ) ) GLOBAL_UNIT_ASSIGNED_CONTEXT ( ( #22086, #8889, #15971 ) ) REPRESENTATION_CONTEXT ( 'NONE', 'WORKASPACE' ) );
#7647=CARTESIAN_POINT ( 'NONE',  ( -2.999999999999996447, 8.485281374238571317, 98.99999999999998579 ) ) ;
#7659=CARTESIAN_POINT ( 'NONE',  ( 0.000000000000000000, 0.000000000000000000, 0.000000000000000000 ) ) ;
#7681=CARTESIAN_POINT ( 'NONE',  ( 0.3931297258116509541, 8.993512908210947288, 78.01929305477952425 ) ) ;
#7688=ORIENTED_EDGE ( 'NONE', *, *, #22699, .F. ) ;
#7791=CARTESIAN_POINT ( 'NONE',  ( 2.257862244182143208, 8.713325772094773214, 79.01511099006255279 ) ) ;
#7811=DIRECTION ( 'NONE',  ( 0.000000000000000000, 0.000000000000000000, 1.000000000000000000 ) ) ;
#7915=ORIENTED_EDGE ( 'NONE', *, *, #3735, .T. ) ;
#7918=EDGE_LOOP ( 'NONE', ( #5709, #5438, #7688, #111 ) ) ;
#8001=VERTEX_POINT ( 'NONE', #11321 ) ;
#8005=AXIS2_PLACEMENT_3D ( 'NONE', #5978, #22344, #13412 ) ;
#8040=EDGE_CURVE ( 'NONE', #21416, #2943, #17680, .T. ) ;
#8153=DIRECTION ( 'NONE',  ( -0.000000000000000000, -0.000000000000000000, -1.000000000000000000 ) ) ;
#8195=APPLICATION_CONTEXT ( 'automotive_design' ) ;
#8246=CARTESIAN_POINT ( 'NONE',  ( -2.999999999999996447, 6.000000000000000000, 98.99999999999998579 ) ) ;
#8250=CONICAL_SURFACE ( 'NONE', #19175, 9.000000000000000000, 0.7853981633974509435 ) ;
#8351=ORIENTED_EDGE ( 'NONE', *, *, #14030, .T. ) ;
#8383=CARTESIAN_POINT ( 'NONE',  ( -2.601798256281209198, 8.616464066528292776, 100.5062743227686752 ) ) ;
#8508=CARTESIAN_POINT ( 'NONE',  ( -2.903219370115622588, 8.518977561982945090, 99.78095984017566877 ) ) ;
#8531=CIRCLE ( 'NONE', #21003, 3.000000000000002665 ) ;
#8571=DIRECTION ( 'NONE',  ( 0.000000000000000000, 0.000000000000000000, 1.000000000000000000 ) ) ;
#8582=CARTESIAN_POINT ( 'NONE',  ( -7.999999999999992895, 0.000000000000000000, 105.0000000000000000 ) ) ;
#8597=LINE ( 'NONE', #2647, #2130 ) ;
#8612=UNCERTAINTY_MEASURE_WITH_UNIT (LENGTH_MEASURE( 1.000000000000000082E-05 ), #22086, 'distance_accuracy_value', 'NONE');
#8664=ORIENTED_EDGE ( 'NONE', *, *, #14514, .T. ) ;
#8677=ORIENTED_EDGE ( 'NONE', *, *, #11026, .T. ) ;
#8861=CARTESIAN_POINT ( 'NONE',  ( -2.258808436415836507, 8.713077898639953744, 100.9837996669589728 ) ) ;
#8889=( NAMED_UNIT ( * ) PLANE_ANGLE_UNIT ( ) SI_UNIT ( $, .RADIAN. ) );
#8938=EDGE_CURVE ( 'NONE', #192, #21201, #9735, .T. ) ;
#8993=ADVANCED_FACE ( 'NONE', ( #17447 ), #8250, .T. ) ;
#9015=FACE_OUTER_BOUND ( 'NONE', #13139, .T. ) ;
#9070=CARTESIAN_POINT ( 'NONE',  ( 3.000000000000000888, 8.485281374238567764, 80.99999999999998579 ) ) ;
#9137=VECTOR ( 'NONE', #15866, 1000.000000000000000 ) ;
#9214=ORIENTED_EDGE ( 'NONE', *, *, #16101, .T. ) ;
#9367=LINE ( 'NONE', #11446, #4951 ) ;
#9407=AXIS2_PLACEMENT_3D ( 'NONE', #5157, #4821, #12587 ) ;
#9582=VERTEX_POINT ( 'NONE', #5925 ) ;
#9636=CARTESIAN_POINT ( 'NONE',  ( 2.383518172110200339, 8.679382520702700887, 79.16775777249439727 ) ) ;
#9639=CARTESIAN_POINT ( 'NONE',  ( -1.335344244249669021, 8.902285279863715317, 78.30632335935361255 ) ) ;
#9698=CARTESIAN_POINT ( 'NONE',  ( 3.000000000000003109, 8.485281374238567764, 98.99999999999998579 ) ) ;
#9735=LINE ( 'NONE', #17193, #10201 ) ;
#9793=DIRECTION ( 'NONE',  ( 1.000000000000000000, 0.000000000000000000, 0.000000000000000000 ) ) ;
#9798=ORIENTED_EDGE ( 'NONE', *, *, #20184, .T. ) ;
#9860=PLANE ( 'NONE',  #15438 ) ;
#10029=DIRECTION ( 'NONE',  ( 0.000000000000000000, -1.000000000000000000, 0.000000000000000000 ) ) ;
#10129=VERTEX_POINT ( 'NONE', #3065 ) ;
#10201=VECTOR ( 'NONE', #19290, 1000.000000000000000 ) ;
#10357=AXIS2_PLACEMENT_3D ( 'NONE', #15786, #10029, #14310 ) ;
#10454=CARTESIAN_POINT ( 'NONE',  ( 1.506443932848089640, 8.874555434635171380, 101.6016380241430568 ) ) ;
#10539=VECTOR ( 'NONE', #4859, 1000.000000000000000 ) ;
#10566=CARTESIAN_POINT ( 'NONE',  ( 9.324366623732823450E-16, 111.0000000000000000, 77.99999999999998579 ) ) ;
#10643=AXIS2_PLACEMENT_3D ( 'NONE', #3591, #20314, #194 ) ;
#10684=CARTESIAN_POINT ( 'NONE',  ( 2.382124412452373274, 8.679761848089601273, 100.8339782245926699 ) ) ;
#10862=EDGE_CURVE ( 'NONE', #6922, #21416, #4115, .T. ) ;
#10898=ORIENTED_EDGE ( 'NONE', *, *, #18486, .T. ) ;
#10936=( LENGTH_UNIT ( ) NAMED_UNIT ( * ) SI_UNIT ( .MILLI., .METRE. ) );
#11026=EDGE_CURVE ( 'NONE', #192, #8001, #14091, .T. ) ;
#11238=VECTOR ( 'NONE', #2750, 1000.000000000000000 ) ;
#11321=CARTESIAN_POINT ( 'NONE',  ( -8.000000000000021316, 1.040949779275251323E-15, 0.000000000000000000 ) ) ;
#11323=DIRECTION ( 'NONE',  ( 0.000000000000000000, 1.000000000000000000, 0.000000000000000000 ) ) ;
#11409=ORIENTED_EDGE ( 'NONE', *, *, #1614, .T. ) ;
#11446=CARTESIAN_POINT ( 'NONE',  ( 7.999999999999992895, 9.797174393178817769E-16, 105.0000000000000000 ) ) ;
#11458=CARTESIAN_POINT ( 'NONE',  ( 2.844687509167349138, 8.538973046698279390, 80.02720063512431636 ) ) ;
#11472=ADVANCED_FACE ( 'NONE', ( #4539 ), #17074, .T. ) ;
#11485=CONICAL_SURFACE ( 'NONE', #5664, 7.999999999999992895, 0.7853981633974439491 ) ;
#11689=DIRECTION ( 'NONE',  ( 1.000000000000000000, 0.000000000000000000, 0.000000000000000000 ) ) ;
#11690=ORIENTED_EDGE ( 'NONE', *, *, #14514, .F. ) ;
#11692=DIRECTION ( 'NONE',  ( -9.637352644315594010E-17, -0.000000000000000000, -1.000000000000000000 ) ) ;
#11698=CARTESIAN_POINT ( 'NONE',  ( -1.508256302856378905, 8.874244307610334559, 78.39942206751072717 ) ) ;
#11814=DIRECTION ( 'NONE',  ( 9.637352644315592778E-17, 0.000000000000000000, 1.000000000000000000 ) ) ;
#11900=DIRECTION ( 'NONE',  ( -0.000000000000000000, -0.000000000000000000, -1.000000000000000000 ) ) ;
#11924=AXIS2_PLACEMENT_3D ( 'NONE', #325, #16768, #15168 ) ;
#11965=FACE_BOUND ( 'NONE', #6475, .T. ) ;
#11971=ORIENTED_EDGE ( 'NONE', *, *, #8938, .T. ) ;
#12025=CARTESIAN_POINT ( 'NONE',  ( 2.844143524245955845, 8.539150930870759382, 99.97419428330140079 ) ) ;
#12078=EDGE_CURVE ( 'NONE', #10129, #9582, #16027, .T. ) ;
#12100=CYLINDRICAL_SURFACE ( 'NONE', #10357, 3.000000000000002665 ) ;
#12148=CARTESIAN_POINT ( 'NONE',  ( -0.7838698549262745896, 8.967904882329030158, 101.9025279484636428 ) ) ;
#12172=PLANE ( 'NONE',  #22583 ) ;
#12238=CARTESIAN_POINT ( 'NONE',  ( 9.324366623732823450E-16, 111.0000000000000000, 80.99999999999998579 ) ) ;
#12244=AXIS2_PLACEMENT_3D ( 'NONE', #24054, #14409, #14660 ) ;
#12340=DIRECTION ( 'NONE',  ( -1.000000000000000000, 0.000000000000000000, 0.000000000000000000 ) ) ;
#12404=CARTESIAN_POINT ( 'NONE',  ( 2.979900905946554435, 8.492461647028314076, 99.39919329559242556 ) ) ;
#12551=CARTESIAN_POINT ( 'NONE',  ( 0.000000000000000000, 0.000000000000000000, 105.0000000000000000 ) ) ;
#12573=EDGE_LOOP ( 'NONE', ( #15136, #22128, #19463, #7915 ) ) ;
#12587=DIRECTION ( 'NONE',  ( 1.000000000000000000, 0.000000000000000000, 0.000000000000000000 ) ) ;
#12599=CIRCLE ( 'NONE', #17289, 9.000000000000000000 ) ;
#12609=AXIS2_PLACEMENT_3D ( 'NONE', #7659, #15099, #5844 ) ;
#12620=DIRECTION ( 'NONE',  ( 0.000000000000000000, 0.000000000000000000, 1.000000000000000000 ) ) ;
#12645=VECTOR ( 'NONE', #4519, 1000.000000000000000 ) ;
#12647=CARTESIAN_POINT ( 'NONE',  ( 9.324366623732823450E-16, 6.000000000000000000, 77.99999999999998579 ) ) ;
#12668=EDGE_CURVE ( 'NONE', #5490, #23000, #17865, .T. ) ;
#13029=ADVANCED_FACE ( 'NONE', ( #18311 ), #11485, .T. ) ;
#13125=EDGE_LOOP ( 'NONE', ( #18848, #11690, #3105, #2237 ) ) ;
#13139=EDGE_LOOP ( 'NONE', ( #4019, #19842, #11971, #17194 ) ) ;
#13155=EDGE_LOOP ( 'NONE', ( #15529, #10898, #13731, #18201 ) ) ;
#13179=CARTESIAN_POINT ( 'NONE',  ( -1.831477161043247870, 8.813213971919513057, 78.61598362702075349 ) ) ;
#13285=VECTOR ( 'NONE', #4974, 1000.000000000000000 ) ;
#13293=CARTESIAN_POINT ( 'NONE',  ( 3.000000000000000888, 8.485281374238567764, 80.80016882425942981 ) ) ;
#13296=CARTESIAN_POINT ( 'NONE',  ( -0.9705301899670187860, 8.949407723703927786, 78.15445800498790163 ) ) ;
#13334=PRODUCT_DEFINITION_CONTEXT ( 'detailed design', #21014, 'design' ) ;
#13359=PLANE ( 'NONE',  #11924 ) ;
#13375=ADVANCED_BREP_SHAPE_REPRESENTATION ( '', ( #2970, #8005 ), #7613 ) ;
#13412=DIRECTION ( 'NONE',  ( 1.000000000000000000, 0.000000000000000000, 0.000000000000000000 ) ) ;
#13439=MECHANICAL_DESIGN_GEOMETRIC_PRESENTATION_REPRESENTATION('',(#1007),#19700);
#13558=CARTESIAN_POINT ( 'NONE',  ( 0.7812760552145768811, 8.968134317516772924, 78.09676514898454514 ) ) ;
#13583=ADVANCED_FACE ( 'NONE', ( #21527 ), #12100, .F. ) ;
#13627=CARTESIAN_POINT ( 'NONE',  ( 8.000000000000021316, 0.000000000000000000, 0.000000000000000000 ) ) ;
#13731=ORIENTED_EDGE ( 'NONE', *, *, #4338, .F. ) ;
#13922=LINE ( 'NONE', #6221, #9137 ) ;
#14004=UNCERTAINTY_MEASURE_WITH_UNIT (LENGTH_MEASURE( 1.000000000000000082E-05 ), #10936, 'distance_accuracy_value', 'NONE');
#14015=ADVANCED_FACE ( 'NONE', ( #4030 ), #9860, .T. ) ;
#14030=EDGE_CURVE ( 'NONE', #14101, #6887, #9367, .T. ) ;
#14075=CYLINDRICAL_SURFACE ( 'NONE', #15332, 3.000000000000002665 ) ;
#14091=CIRCLE ( 'NONE', #22281, 8.000000000000021316 ) ;
#14101=VERTEX_POINT ( 'NONE', #4766 ) ;
#14102=LINE ( 'NONE', #21562, #10539 ) ;
#14117=CARTESIAN_POINT ( 'NONE',  ( -1.847098821903592869, 8.812944685114501908, 101.3956069432029210 ) ) ;
#14123=LINE ( 'NONE', #10566, #12645 ) ;
#14209=CONICAL_SURFACE ( 'NONE', #3696, 9.000000000000000000, 0.7853981633974509435 ) ;
#14235=CARTESIAN_POINT ( 'NONE',  ( -2.999999999999996447, 8.485281374238571317, 98.99999999999998579 ) ) ;
#14310=DIRECTION ( 'NONE',  ( 0.000000000000000000, 0.000000000000000000, -1.000000000000000000 ) ) ;
#14347=CARTESIAN_POINT ( 'NONE',  ( -2.844896095177359197, 8.538902624151456067, 99.97216383474440704 ) ) ;
#14409=DIRECTION ( 'NONE',  ( 0.000000000000000000, 0.000000000000000000, -1.000000000000000000 ) ) ;
#14493=AXIS2_PLACEMENT_3D ( 'NONE', #17190, #8153, #19049 ) ;
#14514=EDGE_CURVE ( 'NONE', #10129, #14101, #20109, .T. ) ;
#14536=AXIS2_PLACEMENT_3D ( 'NONE', #20088, #5322, #3123 ) ;
#14626=CARTESIAN_POINT ( 'NONE',  ( 9.324366632326096311E-16, 9.000000000000000000, 77.99999999999998579 ) ) ;
#14660=DIRECTION ( 'NONE',  ( -1.000000000000000000, 0.000000000000000000, 0.000000000000000000 ) ) ;
#14681=AXIS2_PLACEMENT_3D ( 'NONE', #22612, #7359, #17106 ) ;
#14860=ORIENTED_EDGE ( 'NONE', *, *, #19273, .T. ) ;
#15099=DIRECTION ( 'NONE',  ( 0.000000000000000000, 0.000000000000000000, 1.000000000000000000 ) ) ;
#15118=CARTESIAN_POINT ( 'NONE',  ( 2.980236203076845669, 8.492341138852641080, 80.60398831450446266 ) ) ;
#15136=ORIENTED_EDGE ( 'NONE', *, *, #17180, .F. ) ;
#15168=DIRECTION ( 'NONE',  ( -1.445602896647339163E-16, 0.000000000000000000, -1.000000000000000000 ) ) ;
#15217=CARTESIAN_POINT ( 'NONE',  ( 0.000000000000000000, 0.000000000000000000, 105.0000000000000000 ) ) ;
#15235=CARTESIAN_POINT ( 'NONE',  ( -2.599936666271553509, 8.617022755512742549, 79.49060476457101743 ) ) ;
#15299=ORIENTED_EDGE ( 'NONE', *, *, #96, .F. ) ;
#15332=AXIS2_PLACEMENT_3D ( 'NONE', #12238, #17240, #21035 ) ;
#15438=AXIS2_PLACEMENT_3D ( 'NONE', #15217, #619, #19044 ) ;
#15529=ORIENTED_EDGE ( 'NONE', *, *, #22600, .F. ) ;
#15545=EDGE_LOOP ( 'NONE', ( #9214, #7573, #15716, #20155 ) ) ;
#15598=CARTESIAN_POINT ( 'NONE',  ( 0.000000000000000000, 0.000000000000000000, 0.9999999999999731326 ) ) ;
#15716=ORIENTED_EDGE ( 'NONE', *, *, #6984, .F. ) ;
#15720=DIRECTION ( 'NONE',  ( 0.000000000000000000, 1.000000000000000000, 0.000000000000000000 ) ) ;
#15761=CARTESIAN_POINT ( 'NONE',  ( 0.000000000000000000, 0.000000000000000000, 105.0000000000000000 ) ) ;
#15786=CARTESIAN_POINT ( 'NONE',  ( 3.136800900838523098E-15, 111.0000000000000000, 98.99999999999998579 ) ) ;
#15836=CARTESIAN_POINT ( 'NONE',  ( -2.980262510504976259, 8.492331645729697343, 99.39574783822581594 ) ) ;
#15866=DIRECTION ( 'NONE',  ( 1.445602896647339163E-16, 0.000000000000000000, 1.000000000000000000 ) ) ;
#15948=CARTESIAN_POINT ( 'NONE',  ( 1.982719576835328512, 8.780034855501286373, 101.2598540750001774 ) ) ;
#15971=( NAMED_UNIT ( * ) SI_UNIT ( $, .STERADIAN. ) SOLID_ANGLE_UNIT ( ) );
#16027=LINE ( 'NONE', #8582, #7499 ) ;
#16055=VERTEX_POINT ( 'NONE', #2174 ) ;
#16101=EDGE_CURVE ( 'NONE', #23000, #6922, #5659, .T. ) ;
#16112=DIRECTION ( 'NONE',  ( -1.000000000000000000, 0.000000000000000000, 0.000000000000000000 ) ) ;
#16123=ORIENTED_EDGE ( 'NONE', *, *, #96, .T. ) ;
#16209=EDGE_LOOP ( 'NONE', ( #8677, #2359 ) ) ;
#16319=ORIENTED_EDGE ( 'NONE', *, *, #17024, .T. ) ;
#16342=DIRECTION ( 'NONE',  ( 0.000000000000000000, -1.000000000000000000, 0.000000000000000000 ) ) ;
#16344=DIRECTION ( 'NONE',  ( 0.000000000000000000, 0.000000000000000000, -1.000000000000000000 ) ) ;
#16391=CARTESIAN_POINT ( 'NONE',  ( 0.1973939736642952303, 9.000000000000003553, 78.00000000000000000 ) ) ;
#16419=CARTESIAN_POINT ( 'NONE',  ( 0.000000000000000000, 0.000000000000000000, 103.9999999999999858 ) ) ;
#16459=DIRECTION ( 'NONE',  ( 1.000000000000000000, 0.000000000000000000, 0.000000000000000000 ) ) ;
#16715=ADVANCED_FACE ( 'NONE', ( #3195 ), #16909, .T. ) ;
#16768=DIRECTION ( 'NONE',  ( 1.000000000000000000, 0.000000000000000000, -1.445602896647339163E-16 ) ) ;
#16784=VERTEX_POINT ( 'NONE', #5503 ) ;
#16834=CARTESIAN_POINT ( 'NONE',  ( -2.259833726595073422, 8.712823366420707316, 79.01727130922115805 ) ) ;
#16900=VERTEX_POINT ( 'NONE', #4373 ) ;
#16905=ORIENTED_EDGE ( 'NONE', *, *, #12668, .T. ) ;
#16909=CONICAL_SURFACE ( 'NONE', #12244, 7.999999999999992895, 0.7853981633974439491 ) ;
#16942=VERTEX_POINT ( 'NONE', #8246 ) ;
#16946=CARTESIAN_POINT ( 'NONE',  ( -2.999999999999996447, 111.0000000000000000, 98.99999999999998579 ) ) ;
#16964=CARTESIAN_POINT ( 'NONE',  ( 1.845666383292525525, 8.813255204463377623, 78.60324786774314987 ) ) ;
#17018=SHAPE_REPRESENTATION ( 'Part10^Assembly Drive shaft gear', ( #8005 ), #7613 ) ;
#17022=FACE_OUTER_BOUND ( 'NONE', #18067, .T. ) ;
#17024=EDGE_CURVE ( 'NONE', #5490, #16784, #1918, .T. ) ;
#17074=CYLINDRICAL_SURFACE ( 'NONE', #14493, 9.000000000000000000 ) ;
#17085=CARTESIAN_POINT ( 'NONE',  ( -2.844348310502767152, 8.539081767371294873, 80.02643058434389900 ) ) ;
#17106=DIRECTION ( 'NONE',  ( 1.000000000000000000, 0.000000000000000000, 0.000000000000000000 ) ) ;
#17180=EDGE_CURVE ( 'NONE', #6887, #21201, #8597, .T. ) ;
#17190=CARTESIAN_POINT ( 'NONE',  ( 0.000000000000000000, 0.000000000000000000, 105.0000000000000000 ) ) ;
#17193=CARTESIAN_POINT ( 'NONE',  ( 9.000000000000000000, 0.000000000000000000, 0.9999999999999731326 ) ) ;
#17194=ORIENTED_EDGE ( 'NONE', *, *, #3735, .F. ) ;
#17240=DIRECTION ( 'NONE',  ( 0.000000000000000000, -1.000000000000000000, 0.000000000000000000 ) ) ;
#17285=ORIENTED_EDGE ( 'NONE', *, *, #5248, .T. ) ;
#17289=AXIS2_PLACEMENT_3D ( 'NONE', #5696, #6051, #9793 ) ;
#17336=DIRECTION ( 'NONE',  ( 0.000000000000000000, 0.000000000000000000, 1.000000000000000000 ) ) ;
#17447=FACE_OUTER_BOUND ( 'NONE', #13155, .T. ) ;
#17653=CARTESIAN_POINT ( 'NONE',  ( 3.000000000000003997, 8.485281374238569541, 99.19971821973399528 ) ) ;
#17680=B_SPLINE_CURVE_WITH_KNOTS ( 'NONE', 3,
 ( #9070, #13293, #15118, #4043, #11458, #18934, #2213, #9636, #7791, #16964, #20999, #4178, #13558, #7681, #16391, #5992 ),
 .UNSPECIFIED., .F., .F.,
 ( 4, 2, 2, 2, 2, 2, 2, 4 ),
 ( 0.000000000000000000, 0.0005906230073307718129, 0.001181246014661543626, 0.001771869021992315439, 0.002362492029323087252, 0.003543738043984660368, 0.004134361051315447143, 0.004724984058646233484 ),
 .UNSPECIFIED. ) ;
#17694=ADVANCED_FACE ( 'NONE', ( #6262 ), #14075, .F. ) ;
#17765=CARTESIAN_POINT ( 'NONE',  ( 3.000000000000002665, 111.0000000000000000, 98.99999999999998579 ) ) ;
#17865=LINE ( 'NONE', #1154, #18074 ) ;
#17885=DIRECTION ( 'NONE',  ( 1.000000000000000000, 0.000000000000000000, 0.000000000000000000 ) ) ;
#18067=EDGE_LOOP ( 'NONE', ( #16905, #17285, #4891, #18974 ) ) ;
#18074=VECTOR ( 'NONE', #8571, 1000.000000000000000 ) ;
#18155=CARTESIAN_POINT ( 'NONE',  ( 2.693686482235166046, 8.587799726479698137, 100.3350131173703659 ) ) ;
#18201=ORIENTED_EDGE ( 'NONE', *, *, #8938, .F. ) ;
#18206=VECTOR ( 'NONE', #6860, 1000.000000000000000 ) ;
#18257=ORIENTED_EDGE ( 'NONE', *, *, #12078, .F. ) ;
#18311=FACE_OUTER_BOUND ( 'NONE', #950, .T. ) ;
#18486=EDGE_CURVE ( 'NONE', #8001, #1469, #14102, .T. ) ;
#18542=( NAMED_UNIT ( * ) SI_UNIT ( $, .STERADIAN. ) SOLID_ANGLE_UNIT ( ) );
#18655=( NAMED_UNIT ( * ) PLANE_ANGLE_UNIT ( ) SI_UNIT ( $, .RADIAN. ) );
#18669=CARTESIAN_POINT ( 'NONE',  ( 0.000000000000000000, 0.000000000000000000, 0.9999999999999731326 ) ) ;
#18717=ORIENTED_EDGE ( 'NONE', *, *, #22699, .T. ) ;
#18765=CARTESIAN_POINT ( 'NONE',  ( 9.000000000000000000, 1.102182119232617714E-15, 0.9999999999999731326 ) ) ;
#18848=ORIENTED_EDGE ( 'NONE', *, *, #14030, .F. ) ;
#18877=DIRECTION ( 'NONE',  ( 0.000000000000000000, -1.000000000000000000, 0.000000000000000000 ) ) ;
#18934=CARTESIAN_POINT ( 'NONE',  ( 2.693550685028764491, 8.587845621821196929, 79.66457110399080932 ) ) ;
#18974=ORIENTED_EDGE ( 'NONE', *, *, #17024, .F. ) ;
#19014=ORIENTED_EDGE ( 'NONE', *, *, #6984, .T. ) ;
#19044=DIRECTION ( 'NONE',  ( 1.000000000000000000, 0.000000000000000000, -0.000000000000000000 ) ) ;
#19049=DIRECTION ( 'NONE',  ( -1.000000000000000000, 0.000000000000000000, 0.000000000000000000 ) ) ;
#19175=AXIS2_PLACEMENT_3D ( 'NONE', #15598, #6349, #11689 ) ;
#19178=VECTOR ( 'NONE', #11692, 1000.000000000000000 ) ;
#19190=VERTEX_POINT ( 'NONE', #12647 ) ;
#19191=AXIS2_PLACEMENT_3D ( 'NONE', #15761, #21383, #12340 ) ;
#19230=CARTESIAN_POINT ( 'NONE',  ( 0.000000000000000000, 0.000000000000000000, 0.9999999999999731326 ) ) ;
#19273=EDGE_CURVE ( 'NONE', #9582, #6887, #21908, .T. ) ;
#19290=DIRECTION ( 'NONE',  ( 0.7071067811865493491, 0.000000000000000000, 0.7071067811865456854 ) ) ;
#19433=FACE_OUTER_BOUND ( 'NONE', #7239, .T. ) ;
#19439=DIRECTION ( 'NONE',  ( 1.000000000000000000, 0.000000000000000000, 0.000000000000000000 ) ) ;
#19463=ORIENTED_EDGE ( 'NONE', *, *, #24070, .T. ) ;
#19465=ORIENTED_EDGE ( 'NONE', *, *, #21, .T. ) ;
#19500=CARTESIAN_POINT ( 'NONE',  ( 1.830024671936552272, 8.813519001246380213, 101.3851422246032570 ) ) ;
#19511=ORIENTED_EDGE ( 'NONE', *, *, #17180, .T. ) ;
#19627=CARTESIAN_POINT ( 'NONE',  ( 2.599411561834574336, 8.617182949674106140, 100.5103153236600519 ) ) ;
#19659=CARTESIAN_POINT ( 'NONE',  ( 3.000000000000000888, 111.0000000000000000, 80.99999999999998579 ) ) ;
#19700=( GEOMETRIC_REPRESENTATION_CONTEXT ( 3 ) GLOBAL_UNCERTAINTY_ASSIGNED_CONTEXT ( ( #14004 ) ) GLOBAL_UNIT_ASSIGNED_CONTEXT ( ( #10936, #18655, #18542 ) ) REPRESENTATION_CONTEXT ( 'NONE', 'WORKASPACE' ) );
#19714=AXIS2_PLACEMENT_3D ( 'NONE', #19659, #4401, #11814 ) ;
#19805=LINE ( 'NONE', #3077, #18206 ) ;
#19842=ORIENTED_EDGE ( 'NONE', *, *, #11026, .F. ) ;
#19863=CARTESIAN_POINT ( 'NONE',  ( 0.9681541731161901199, 8.949668379605448365, 101.8463591495539333 ) ) ;
#19869=DIRECTION ( 'NONE',  ( 1.000000000000000000, 0.000000000000000000, 0.000000000000000000 ) ) ;
#20085=DIRECTION ( 'NONE',  ( 1.000000000000000000, 0.000000000000000000, 0.000000000000000000 ) ) ;
#20088=CARTESIAN_POINT ( 'NONE',  ( 3.136800900838523098E-15, 6.000000000000000000, 98.99999999999998579 ) ) ;
#20109=CIRCLE ( 'NONE', #4532, 7.999999999999992895 ) ;
#20155=ORIENTED_EDGE ( 'NONE', *, *, #5248, .F. ) ;
#20184=EDGE_CURVE ( 'NONE', #21416, #16900, #5377, .T. ) ;
#20301=ADVANCED_FACE ( 'NONE', ( #2306 ), #4152, .F. ) ;
#20314=DIRECTION ( 'NONE',  ( 0.000000000000000000, -1.000000000000000000, 0.000000000000000000 ) ) ;
#20498=CARTESIAN_POINT ( 'NONE',  ( 3.000000000000000888, 111.0000000000000000, 80.99999999999998579 ) ) ;
#20559=DIRECTION ( 'NONE',  ( -0.000000000000000000, -0.000000000000000000, -1.000000000000000000 ) ) ;
#20638=CARTESIAN_POINT ( 'NONE',  ( -2.901769741831041305, 8.519474286710609690, 80.21333227949575928 ) ) ;
#20665=EDGE_CURVE ( 'NONE', #2943, #19190, #14123, .T. ) ;
#20876=DIRECTION ( 'NONE',  ( 0.7071067811865444641, 8.659560562354895880E-17, -0.7071067811865505703 ) ) ;
#20893=CARTESIAN_POINT ( 'NONE',  ( -2.999999999999999112, 8.485281374238567764, 80.99999999999998579 ) ) ;
#20951=CARTESIAN_POINT ( 'NONE',  ( 3.000000000000003109, 8.485281374238567764, 105.0000000000000000 ) ) ;
#20999=CARTESIAN_POINT ( 'NONE',  ( 1.513123620469492447, 8.879344224389656759, 78.38024625474098173 ) ) ;
#21003=AXIS2_PLACEMENT_3D ( 'NONE', #4182, #11323, #17336 ) ;
#21014=APPLICATION_CONTEXT ( 'automotive_design' ) ;
#21018=CARTESIAN_POINT ( 'NONE',  ( 9.324366623732823450E-16, 6.000000000000000000, 80.99999999999998579 ) ) ;
#21035=DIRECTION ( 'NONE',  ( 0.000000000000000000, 0.000000000000000000, -1.000000000000000000 ) ) ;
#21108=LINE ( 'NONE', #5758, #19178 ) ;
#21201=VERTEX_POINT ( 'NONE', #18765 ) ;
#21247=PRODUCT_DEFINITION ( 'UNKNOWN', '', #6092, #13334 ) ;
#21271=CARTESIAN_POINT ( 'NONE',  ( 0.000000000000000000, 0.000000000000000000, 0.000000000000000000 ) ) ;
#21336=CARTESIAN_POINT ( 'NONE',  ( -0.2004283449780275561, 8.999929632622238884, 101.9997888977613911 ) ) ;
#21369=ORIENTED_EDGE ( 'NONE', *, *, #16101, .F. ) ;
#21383=DIRECTION ( 'NONE',  ( -0.000000000000000000, -0.000000000000000000, -1.000000000000000000 ) ) ;
#21416=VERTEX_POINT ( 'NONE', #7324 ) ;
#21527=FACE_OUTER_BOUND ( 'NONE', #15545, .T. ) ;
#21562=CARTESIAN_POINT ( 'NONE',  ( -9.000000000000000000, 1.102182119232617714E-15, 0.9999999999999731326 ) ) ;
#21577=CARTESIAN_POINT ( 'NONE',  ( 2.258892838145987181, 8.713070189660834686, 100.9838146350991934 ) ) ;
#21732=ADVANCED_FACE ( 'NONE', ( #739 ), #2436, .T. ) ;
#21807=CARTESIAN_POINT ( 'NONE',  ( -1.514930817284593445, 8.879021050564452011, 101.6186676026875233 ) ) ;
#21892=ORIENTED_EDGE ( 'NONE', *, *, #2690, .T. ) ;
#21908=CIRCLE ( 'NONE', #3980, 9.000000000000000000 ) ;
#22026=DIRECTION ( 'NONE',  ( -0.7071067811865444641, 0.000000000000000000, -0.7071067811865505703 ) ) ;
#22086=( LENGTH_UNIT ( ) NAMED_UNIT ( * ) SI_UNIT ( .MILLI., .METRE. ) );
#22104=ORIENTED_EDGE ( 'NONE', *, *, #20665, .F. ) ;
#22114=DIRECTION ( 'NONE',  ( 0.000000000000000000, -1.000000000000000000, 0.000000000000000000 ) ) ;
#22128=ORIENTED_EDGE ( 'NONE', *, *, #4058, .T. ) ;
#22281=AXIS2_PLACEMENT_3D ( 'NONE', #5318, #20559, #3361 ) ;
#22344=DIRECTION ( 'NONE',  ( 0.000000000000000000, 0.000000000000000000, 1.000000000000000000 ) ) ;
#22402=VECTOR ( 'NONE', #18877, 1000.000000000000000 ) ;
#22487=CARTESIAN_POINT ( 'NONE',  ( -2.694088866357877254, 8.587672555557725573, 79.66581864099087795 ) ) ;
#22523=PRODUCT_CONTEXT ( 'NONE', #8195, 'mechanical' ) ;
#22583=AXIS2_PLACEMENT_3D ( 'NONE', #4645, #15720, #614 ) ;
#22589=CARTESIAN_POINT ( 'NONE',  ( -0.1971285389010652422, 9.000000000000000000, 77.99999999999998579 ) ) ;
#22600=EDGE_CURVE ( 'NONE', #8001, #192, #23613, .T. ) ;
#22612=CARTESIAN_POINT ( 'NONE',  ( 0.000000000000000000, 0.000000000000000000, 103.9999999999999858 ) ) ;
#22699=EDGE_CURVE ( 'NONE', #16900, #19190, #23978, .T. ) ;
#22817=ORIENTED_EDGE ( 'NONE', *, *, #10862, .T. ) ;
#22986=ORIENTED_EDGE ( 'NONE', *, *, #21, .F. ) ;
#22990=CARTESIAN_POINT ( 'NONE',  ( -2.999999999999999112, 8.485281374238567764, 80.99999999999998579 ) ) ;
#23000=VERTEX_POINT ( 'NONE', #7647 ) ;
#23094=ORIENTED_EDGE ( 'NONE', *, *, #4338, .T. ) ;
#23297=CARTESIAN_POINT ( 'NONE',  ( -2.999999999999995559, 8.485281374238571317, 99.19969681971174680 ) ) ;
#23331=ORIENTED_EDGE ( 'NONE', *, *, #24070, .F. ) ;
#23411=CARTESIAN_POINT ( 'NONE',  ( -0.9743949605962830551, 8.948941949199685553, 101.8440575432637587 ) ) ;
#23558=ADVANCED_FACE ( 'NONE', ( #17022 ), #13359, .T. ) ;
#23613=CIRCLE ( 'NONE', #7270, 8.000000000000021316 ) ;
#23978=CIRCLE ( 'NONE', #7212, 3.000000000000002665 ) ;
#24054=CARTESIAN_POINT ( 'NONE',  ( 0.000000000000000000, 0.000000000000000000, 105.0000000000000000 ) ) ;
#24070=EDGE_CURVE ( 'NONE', #9582, #1469, #19805, .T. ) ;
#24149=COLOUR_RGB('Grey',0.48,0.52,0.57);
#24150=FILL_AREA_STYLE_COLOUR('',#24149);
#24151=FILL_AREA_STYLE('',(#24150));
#24152=SURFACE_STYLE_FILL_AREA(#24151);
#24153=SURFACE_SIDE_STYLE('',(#24152));
#24154=SURFACE_STYLE_USAGE(.BOTH.,#24153);
#24155=PRESENTATION_STYLE_ASSIGNMENT((#24154));
ENDSEC;
END-ISO-10303-21;
